ISO-10303-21;
HEADER;
/* Generated by software containing ST-Developer
 * from STEP Tools, Inc. (www.steptools.com) 
 */

FILE_DESCRIPTION(
/* description */ ('Two-link friction support arm'),
/* implementation_level */ '2;1');

FILE_NAME(
/* name */ 'M5x14 Cap Screw.step',
/* time_stamp */ '2026-10-27T20:01:49-07:00',
/* author */ (''),
/* organization */ (''),
/* preprocessor_version */ 'ST-DEVELOPER v20.2',
/* originating_system */ 'Autodesk Translation Framework v15.17.0.0',
/* authorisation */ '');

FILE_SCHEMA (('AUTOMOTIVE_DESIGN { 1 0 10303 214 3 1 1 }'));
ENDSEC;

DATA;
#10=MECHANICAL_DESIGN_GEOMETRIC_PRESENTATION_REPRESENTATION('',(#199),#5492);
#161=ORIENTED_CLOSED_SHELL('',*,#3175,.F.);
#162=BREP_WITH_VOIDS('Body1',#3176,(#161));
#164=CONICAL_SURFACE('',#3422,0.4,0.785398163397448);
#165=CONICAL_SURFACE('',#3426,0.41,0.785398163397448);
#166=CONICAL_SURFACE('',#3430,0.26,0.463647609000806);
#177=SHAPE_REPRESENTATION_RELATIONSHIP('SRR','None',#5568,#188);
#188=ADVANCED_BREP_SHAPE_REPRESENTATION('',(#162),#5482);
#199=STYLED_ITEM('',(#5708),#162);
#227=FACE_BOUND('',#644,.T.);
#321=PLANE('',#3410);
#322=PLANE('',#3411);
#323=PLANE('',#3412);
#324=PLANE('',#3413);
#325=PLANE('',#3414);
#326=PLANE('',#3415);
#327=PLANE('',#3416);
#328=PLANE('',#3417);
#329=PLANE('',#3418);
#330=PLANE('',#3420);
#331=PLANE('',#3428);
#452=FACE_OUTER_BOUND('',#630,.T.);
#453=FACE_OUTER_BOUND('',#631,.T.);
#454=FACE_OUTER_BOUND('',#632,.T.);
#455=FACE_OUTER_BOUND('',#633,.T.);
#456=FACE_OUTER_BOUND('',#634,.T.);
#457=FACE_OUTER_BOUND('',#635,.T.);
#458=FACE_OUTER_BOUND('',#636,.T.);
#459=FACE_OUTER_BOUND('',#637,.T.);
#460=FACE_OUTER_BOUND('',#638,.T.);
#461=FACE_OUTER_BOUND('',#639,.T.);
#462=FACE_OUTER_BOUND('',#640,.T.);
#463=FACE_OUTER_BOUND('',#641,.T.);
#464=FACE_OUTER_BOUND('',#642,.T.);
#465=FACE_OUTER_BOUND('',#643,.T.);
#466=FACE_OUTER_BOUND('',#645,.T.);
#467=FACE_OUTER_BOUND('',#646,.T.);
#630=EDGE_LOOP('',(#2568,#2569,#2570,#2571));
#631=EDGE_LOOP('',(#2572,#2573,#2574,#2575));
#632=EDGE_LOOP('',(#2576,#2577,#2578,#2579));
#633=EDGE_LOOP('',(#2580,#2581,#2582,#2583));
#634=EDGE_LOOP('',(#2584,#2585,#2586,#2587));
#635=EDGE_LOOP('',(#2588,#2589,#2590,#2591));
#636=EDGE_LOOP('',(#2592,#2593,#2594,#2595,#2596,#2597));
#637=EDGE_LOOP('',(#2598,#2599,#2600,#2601,#2602,#2603));
#638=EDGE_LOOP('',(#2604));
#639=EDGE_LOOP('',(#2605));
#640=EDGE_LOOP('',(#2606,#2607,#2608,#2609));
#641=EDGE_LOOP('',(#2610,#2611,#2612,#2613));
#642=EDGE_LOOP('',(#2614,#2615,#2616,#2617));
#643=EDGE_LOOP('',(#2618));
#644=EDGE_LOOP('',(#2619));
#645=EDGE_LOOP('',(#2620,#2621,#2622,#2623));
#646=EDGE_LOOP('',(#2624,#2625,#2626,#2627));
#937=LINE('',#4965,#1250);
#938=LINE('',#4967,#1251);
#939=LINE('',#4969,#1252);
#940=LINE('',#4970,#1253);
#941=LINE('',#4973,#1254);
#942=LINE('',#4975,#1255);
#943=LINE('',#4976,#1256);
#944=LINE('',#4979,#1257);
#945=LINE('',#4981,#1258);
#946=LINE('',#4982,#1259);
#947=LINE('',#4985,#1260);
#948=LINE('',#4987,#1261);
#949=LINE('',#4988,#1262);
#950=LINE('',#4991,#1263);
#951=LINE('',#4993,#1264);
#952=LINE('',#4994,#1265);
#953=LINE('',#4996,#1266);
#954=LINE('',#4997,#1267);
#955=LINE('',#5009,#1268);
#956=LINE('',#5013,#1269);
#957=LINE('',#5017,#1270);
#958=LINE('',#5024,#1271);
#959=LINE('',#5026,#1272);
#1250=VECTOR('',#4013,1.);
#1251=VECTOR('',#4014,1.);
#1252=VECTOR('',#4015,1.);
#1253=VECTOR('',#4016,1.);
#1254=VECTOR('',#4019,1.);
#1255=VECTOR('',#4020,1.);
#1256=VECTOR('',#4021,1.);
#1257=VECTOR('',#4024,1.);
#1258=VECTOR('',#4025,1.);
#1259=VECTOR('',#4026,1.);
#1260=VECTOR('',#4029,1.);
#1261=VECTOR('',#4030,1.);
#1262=VECTOR('',#4031,1.);
#1263=VECTOR('',#4034,1.);
#1264=VECTOR('',#4035,1.);
#1265=VECTOR('',#4036,1.);
#1266=VECTOR('',#4039,1.);
#1267=VECTOR('',#4040,1.);
#1268=VECTOR('',#4057,0.4);
#1269=VECTOR('',#4062,0.425);
#1270=VECTOR('',#4067,0.41);
#1271=VECTOR('',#4076,0.26);
#1272=VECTOR('',#4079,0.25);
#1384=CIRCLE('',#3419,0.24505);
#1385=CIRCLE('',#3421,0.375);
#1386=CIRCLE('',#3423,0.425);
#1387=CIRCLE('',#3425,0.425);
#1388=CIRCLE('',#3427,0.395);
#1389=CIRCLE('',#3429,0.27);
#1390=CIRCLE('',#3431,0.24505);
#1592=VERTEX_POINT('',#4963);
#1593=VERTEX_POINT('',#4964);
#1594=VERTEX_POINT('',#4966);
#1595=VERTEX_POINT('',#4968);
#1596=VERTEX_POINT('',#4972);
#1597=VERTEX_POINT('',#4974);
#1598=VERTEX_POINT('',#4978);
#1599=VERTEX_POINT('',#4980);
#1600=VERTEX_POINT('',#4984);
#1601=VERTEX_POINT('',#4986);
#1602=VERTEX_POINT('',#4990);
#1603=VERTEX_POINT('',#4992);
#1604=VERTEX_POINT('',#5001);
#1605=VERTEX_POINT('',#5004);
#1606=VERTEX_POINT('',#5007);
#1607=VERTEX_POINT('',#5011);
#1608=VERTEX_POINT('',#5015);
#1609=VERTEX_POINT('',#5019);
#1610=VERTEX_POINT('',#5022);
#1938=EDGE_CURVE('',#1592,#1593,#937,.T.);
#1939=EDGE_CURVE('',#1593,#1594,#938,.T.);
#1940=EDGE_CURVE('',#1594,#1595,#939,.T.);
#1941=EDGE_CURVE('',#1592,#1595,#940,.T.);
#1942=EDGE_CURVE('',#1593,#1596,#941,.T.);
#1943=EDGE_CURVE('',#1596,#1597,#942,.T.);
#1944=EDGE_CURVE('',#1597,#1594,#943,.T.);
#1945=EDGE_CURVE('',#1596,#1598,#944,.T.);
#1946=EDGE_CURVE('',#1598,#1599,#945,.T.);
#1947=EDGE_CURVE('',#1599,#1597,#946,.T.);
#1948=EDGE_CURVE('',#1598,#1600,#947,.T.);
#1949=EDGE_CURVE('',#1600,#1601,#948,.T.);
#1950=EDGE_CURVE('',#1601,#1599,#949,.T.);
#1951=EDGE_CURVE('',#1600,#1602,#950,.T.);
#1952=EDGE_CURVE('',#1602,#1603,#951,.T.);
#1953=EDGE_CURVE('',#1603,#1601,#952,.T.);
#1954=EDGE_CURVE('',#1602,#1592,#953,.T.);
#1955=EDGE_CURVE('',#1595,#1603,#954,.T.);
#1956=EDGE_CURVE('',#1604,#1604,#1384,.T.);
#1957=EDGE_CURVE('',#1605,#1605,#1385,.T.);
#1958=EDGE_CURVE('',#1606,#1606,#1386,.T.);
#1959=EDGE_CURVE('',#1606,#1605,#955,.T.);
#1960=EDGE_CURVE('',#1607,#1607,#1387,.T.);
#1961=EDGE_CURVE('',#1607,#1606,#956,.T.);
#1962=EDGE_CURVE('',#1608,#1608,#1388,.T.);
#1963=EDGE_CURVE('',#1608,#1607,#957,.T.);
#1964=EDGE_CURVE('',#1609,#1609,#1389,.T.);
#1965=EDGE_CURVE('',#1610,#1610,#1390,.F.);
#1966=EDGE_CURVE('',#1610,#1609,#958,.T.);
#1967=EDGE_CURVE('',#1604,#1610,#959,.T.);
#2568=ORIENTED_EDGE('',*,*,#1938,.T.);
#2569=ORIENTED_EDGE('',*,*,#1939,.T.);
#2570=ORIENTED_EDGE('',*,*,#1940,.T.);
#2571=ORIENTED_EDGE('',*,*,#1941,.F.);
#2572=ORIENTED_EDGE('',*,*,#1942,.T.);
#2573=ORIENTED_EDGE('',*,*,#1943,.T.);
#2574=ORIENTED_EDGE('',*,*,#1944,.T.);
#2575=ORIENTED_EDGE('',*,*,#1939,.F.);
#2576=ORIENTED_EDGE('',*,*,#1945,.T.);
#2577=ORIENTED_EDGE('',*,*,#1946,.T.);
#2578=ORIENTED_EDGE('',*,*,#1947,.T.);
#2579=ORIENTED_EDGE('',*,*,#1943,.F.);
#2580=ORIENTED_EDGE('',*,*,#1948,.T.);
#2581=ORIENTED_EDGE('',*,*,#1949,.T.);
#2582=ORIENTED_EDGE('',*,*,#1950,.T.);
#2583=ORIENTED_EDGE('',*,*,#1946,.F.);
#2584=ORIENTED_EDGE('',*,*,#1951,.T.);
#2585=ORIENTED_EDGE('',*,*,#1952,.T.);
#2586=ORIENTED_EDGE('',*,*,#1953,.T.);
#2587=ORIENTED_EDGE('',*,*,#1949,.F.);
#2588=ORIENTED_EDGE('',*,*,#1954,.T.);
#2589=ORIENTED_EDGE('',*,*,#1941,.T.);
#2590=ORIENTED_EDGE('',*,*,#1955,.T.);
#2591=ORIENTED_EDGE('',*,*,#1952,.F.);
#2592=ORIENTED_EDGE('',*,*,#1954,.F.);
#2593=ORIENTED_EDGE('',*,*,#1951,.F.);
#2594=ORIENTED_EDGE('',*,*,#1948,.F.);
#2595=ORIENTED_EDGE('',*,*,#1945,.F.);
#2596=ORIENTED_EDGE('',*,*,#1942,.F.);
#2597=ORIENTED_EDGE('',*,*,#1938,.F.);
#2598=ORIENTED_EDGE('',*,*,#1955,.F.);
#2599=ORIENTED_EDGE('',*,*,#1940,.F.);
#2600=ORIENTED_EDGE('',*,*,#1944,.F.);
#2601=ORIENTED_EDGE('',*,*,#1947,.F.);
#2602=ORIENTED_EDGE('',*,*,#1950,.F.);
#2603=ORIENTED_EDGE('',*,*,#1953,.F.);
#2604=ORIENTED_EDGE('',*,*,#1956,.F.);
#2605=ORIENTED_EDGE('',*,*,#1957,.F.);
#2606=ORIENTED_EDGE('',*,*,#1958,.F.);
#2607=ORIENTED_EDGE('',*,*,#1959,.T.);
#2608=ORIENTED_EDGE('',*,*,#1957,.T.);
#2609=ORIENTED_EDGE('',*,*,#1959,.F.);
#2610=ORIENTED_EDGE('',*,*,#1960,.F.);
#2611=ORIENTED_EDGE('',*,*,#1961,.T.);
#2612=ORIENTED_EDGE('',*,*,#1958,.T.);
#2613=ORIENTED_EDGE('',*,*,#1961,.F.);
#2614=ORIENTED_EDGE('',*,*,#1962,.F.);
#2615=ORIENTED_EDGE('',*,*,#1963,.T.);
#2616=ORIENTED_EDGE('',*,*,#1960,.T.);
#2617=ORIENTED_EDGE('',*,*,#1963,.F.);
#2618=ORIENTED_EDGE('',*,*,#1962,.T.);
#2619=ORIENTED_EDGE('',*,*,#1964,.F.);
#2620=ORIENTED_EDGE('',*,*,#1965,.F.);
#2621=ORIENTED_EDGE('',*,*,#1966,.T.);
#2622=ORIENTED_EDGE('',*,*,#1964,.T.);
#2623=ORIENTED_EDGE('',*,*,#1966,.F.);
#2624=ORIENTED_EDGE('',*,*,#1956,.T.);
#2625=ORIENTED_EDGE('',*,*,#1967,.T.);
#2626=ORIENTED_EDGE('',*,*,#1965,.T.);
#2627=ORIENTED_EDGE('',*,*,#1967,.F.);
#2975=CYLINDRICAL_SURFACE('',#3424,0.425);
#2976=CYLINDRICAL_SURFACE('',#3432,0.24505);
#3083=ADVANCED_FACE('',(#452),#321,.F.);
#3084=ADVANCED_FACE('',(#453),#322,.F.);
#3085=ADVANCED_FACE('',(#454),#323,.F.);
#3086=ADVANCED_FACE('',(#455),#324,.F.);
#3087=ADVANCED_FACE('',(#456),#325,.F.);
#3088=ADVANCED_FACE('',(#457),#326,.F.);
#3089=ADVANCED_FACE('',(#458),#327,.F.);
#3090=ADVANCED_FACE('',(#459),#328,.F.);
#3091=ADVANCED_FACE('',(#460),#329,.F.);
#3092=ADVANCED_FACE('',(#461),#330,.T.);
#3093=ADVANCED_FACE('',(#462),#164,.T.);
#3094=ADVANCED_FACE('',(#463),#2975,.T.);
#3095=ADVANCED_FACE('',(#464),#165,.T.);
#3096=ADVANCED_FACE('',(#465,#227),#331,.T.);
#3097=ADVANCED_FACE('',(#466),#166,.T.);
#3098=ADVANCED_FACE('',(#467),#2976,.T.);
#3175=CLOSED_SHELL('',(#3083,#3084,#3085,#3086,#3087,#3088,#3089,#3090));
#3176=CLOSED_SHELL('',(#3091,#3092,#3093,#3094,#3095,#3096,#3097,#3098));
#3409=AXIS2_PLACEMENT_3D('',#4961,#4009,#4010);
#3410=AXIS2_PLACEMENT_3D('',#4962,#4011,#4012);
#3411=AXIS2_PLACEMENT_3D('',#4971,#4017,#4018);
#3412=AXIS2_PLACEMENT_3D('',#4977,#4022,#4023);
#3413=AXIS2_PLACEMENT_3D('',#4983,#4027,#4028);
#3414=AXIS2_PLACEMENT_3D('',#4989,#4032,#4033);
#3415=AXIS2_PLACEMENT_3D('',#4995,#4037,#4038);
#3416=AXIS2_PLACEMENT_3D('',#4998,#4041,#4042);
#3417=AXIS2_PLACEMENT_3D('',#4999,#4043,#4044);
#3418=AXIS2_PLACEMENT_3D('',#5000,#4045,#4046);
#3419=AXIS2_PLACEMENT_3D('',#5002,#4047,#4048);
#3420=AXIS2_PLACEMENT_3D('',#5003,#4049,#4050);
#3421=AXIS2_PLACEMENT_3D('',#5005,#4051,#4052);
#3422=AXIS2_PLACEMENT_3D('',#5006,#4053,#4054);
#3423=AXIS2_PLACEMENT_3D('',#5008,#4055,#4056);
#3424=AXIS2_PLACEMENT_3D('',#5010,#4058,#4059);
#3425=AXIS2_PLACEMENT_3D('',#5012,#4060,#4061);
#3426=AXIS2_PLACEMENT_3D('',#5014,#4063,#4064);
#3427=AXIS2_PLACEMENT_3D('',#5016,#4065,#4066);
#3428=AXIS2_PLACEMENT_3D('',#5018,#4068,#4069);
#3429=AXIS2_PLACEMENT_3D('',#5020,#4070,#4071);
#3430=AXIS2_PLACEMENT_3D('',#5021,#4072,#4073);
#3431=AXIS2_PLACEMENT_3D('',#5023,#4074,#4075);
#3432=AXIS2_PLACEMENT_3D('',#5025,#4077,#4078);
#4009=DIRECTION('axis',(0.,0.,1.));
#4010=DIRECTION('refdir',(1.,0.,0.));
#4011=DIRECTION('center_axis',(0.866025403784439,0.,-0.5));
#4012=DIRECTION('ref_axis',(0.5,0.,0.866025403784439));
#4013=DIRECTION('',(-0.5,0.,-0.866025403784439));
#4014=DIRECTION('',(0.,-1.,0.));
#4015=DIRECTION('',(0.5,0.,0.866025403784439));
#4016=DIRECTION('',(0.,-1.,0.));
#4017=DIRECTION('center_axis',(1.20185167898973E-16,0.,-1.));
#4018=DIRECTION('ref_axis',(1.,0.,1.20185167898973E-16));
#4019=DIRECTION('',(-1.,0.,-1.20185167898973E-16));
#4020=DIRECTION('',(0.,-1.,0.));
#4021=DIRECTION('',(1.,0.,1.20185167898973E-16));
#4022=DIRECTION('center_axis',(-0.866025403784439,0.,-0.5));
#4023=DIRECTION('ref_axis',(0.5,0.,-0.866025403784439));
#4024=DIRECTION('',(-0.5,0.,0.866025403784439));
#4025=DIRECTION('',(0.,-1.,0.));
#4026=DIRECTION('',(0.5,0.,-0.866025403784439));
#4027=DIRECTION('center_axis',(-0.866025403784439,0.,0.5));
#4028=DIRECTION('ref_axis',(-0.5,0.,-0.866025403784439));
#4029=DIRECTION('',(0.5,0.,0.866025403784439));
#4030=DIRECTION('',(0.,-1.,0.));
#4031=DIRECTION('',(-0.5,0.,-0.866025403784439));
#4032=DIRECTION('center_axis',(-2.40370335797945E-16,0.,1.));
#4033=DIRECTION('ref_axis',(-1.,0.,-2.40370335797945E-16));
#4034=DIRECTION('',(1.,0.,2.40370335797945E-16));
#4035=DIRECTION('',(0.,-1.,0.));
#4036=DIRECTION('',(-1.,0.,-2.40370335797945E-16));
#4037=DIRECTION('center_axis',(0.866025403784439,0.,0.5));
#4038=DIRECTION('ref_axis',(-0.5,0.,0.866025403784439));
#4039=DIRECTION('',(0.5,0.,-0.866025403784439));
#4040=DIRECTION('',(-0.5,0.,0.866025403784439));
#4041=DIRECTION('center_axis',(0.,1.,0.));
#4042=DIRECTION('ref_axis',(1.,0.,0.));
#4043=DIRECTION('center_axis',(0.,-1.,0.));
#4044=DIRECTION('ref_axis',(0.,0.,-1.));
#4045=DIRECTION('center_axis',(0.,1.,0.));
#4046=DIRECTION('ref_axis',(1.,0.,0.));
#4047=DIRECTION('center_axis',(0.,1.,0.));
#4048=DIRECTION('ref_axis',(1.,0.,0.));
#4049=DIRECTION('center_axis',(0.,1.,0.));
#4050=DIRECTION('ref_axis',(0.,0.,1.));
#4051=DIRECTION('center_axis',(0.,-1.,0.));
#4052=DIRECTION('ref_axis',(1.,0.,0.));
#4053=DIRECTION('center_axis',(0.,-1.,0.));
#4054=DIRECTION('ref_axis',(1.,0.,0.));
#4055=DIRECTION('center_axis',(0.,-1.,0.));
#4056=DIRECTION('ref_axis',(1.,0.,0.));
#4057=DIRECTION('',(0.707106781186548,0.707106781186547,8.65956056235493E-17));
#4058=DIRECTION('center_axis',(0.,-1.,0.));
#4059=DIRECTION('ref_axis',(1.,0.,0.));
#4060=DIRECTION('center_axis',(0.,-1.,0.));
#4061=DIRECTION('ref_axis',(1.,0.,0.));
#4062=DIRECTION('',(0.,1.,0.));
#4063=DIRECTION('center_axis',(0.,1.,0.));
#4064=DIRECTION('ref_axis',(1.,0.,0.));
#4065=DIRECTION('center_axis',(0.,-1.,0.));
#4066=DIRECTION('ref_axis',(1.,0.,0.));
#4067=DIRECTION('',(-0.707106781186547,0.707106781186548,-8.65956056235493E-17));
#4068=DIRECTION('center_axis',(0.,-1.,0.));
#4069=DIRECTION('ref_axis',(0.,0.,-1.));
#4070=DIRECTION('center_axis',(0.,-1.,0.));
#4071=DIRECTION('ref_axis',(1.,0.,0.));
#4072=DIRECTION('center_axis',(0.,1.,0.));
#4073=DIRECTION('ref_axis',(1.,0.,0.));
#4074=DIRECTION('center_axis',(0.,1.,0.));
#4075=DIRECTION('ref_axis',(1.,0.,0.));
#4076=DIRECTION('',(-0.447213595499958,0.894427190999916,-5.47678698264203E-17));
#4077=DIRECTION('center_axis',(0.,-1.,0.));
#4078=DIRECTION('ref_axis',(1.,0.,0.));
#4079=DIRECTION('',(0.,1.,0.));
#4961=CARTESIAN_POINT('',(0.,0.,0.));
#4962=CARTESIAN_POINT('Origin',(0.115470053837925,-0.5,-0.2));
#4963=CARTESIAN_POINT('',(0.23094010767585,-0.5,0.));
#4964=CARTESIAN_POINT('',(0.115470053837925,-0.5,-0.2));
#4965=CARTESIAN_POINT('',(0.23094010767585,-0.5,0.));
#4966=CARTESIAN_POINT('',(0.115470053837925,-0.8,-0.2));
#4967=CARTESIAN_POINT('',(0.115470053837925,-0.5,-0.2));
#4968=CARTESIAN_POINT('',(0.23094010767585,-0.8,0.));
#4969=CARTESIAN_POINT('',(0.23094010767585,-0.8,0.));
#4970=CARTESIAN_POINT('',(0.23094010767585,-0.5,0.));
#4971=CARTESIAN_POINT('Origin',(-0.115470053837925,-0.5,-0.2));
#4972=CARTESIAN_POINT('',(-0.115470053837925,-0.5,-0.2));
#4973=CARTESIAN_POINT('',(0.115470053837925,-0.5,-0.2));
#4974=CARTESIAN_POINT('',(-0.115470053837925,-0.8,-0.2));
#4975=CARTESIAN_POINT('',(-0.115470053837925,-0.5,-0.2));
#4976=CARTESIAN_POINT('',(0.115470053837925,-0.8,-0.2));
#4977=CARTESIAN_POINT('Origin',(-0.23094010767585,-0.5,-2.77555756156289E-17));
#4978=CARTESIAN_POINT('',(-0.23094010767585,-0.5,-2.82820063659975E-17));
#4979=CARTESIAN_POINT('',(-0.115470053837925,-0.5,-0.2));
#4980=CARTESIAN_POINT('',(-0.23094010767585,-0.8,-2.77555756156289E-17));
#4981=CARTESIAN_POINT('',(-0.23094010767585,-0.5,-2.82820063659975E-17));
#4982=CARTESIAN_POINT('',(-0.115470053837925,-0.8,-0.2));
#4983=CARTESIAN_POINT('Origin',(-0.115470053837925,-0.5,0.2));
#4984=CARTESIAN_POINT('',(-0.115470053837925,-0.5,0.2));
#4985=CARTESIAN_POINT('',(-0.23094010767585,-0.5,-2.82820063659975E-17));
#4986=CARTESIAN_POINT('',(-0.115470053837925,-0.8,0.2));
#4987=CARTESIAN_POINT('',(-0.115470053837925,-0.5,0.2));
#4988=CARTESIAN_POINT('',(-0.23094010767585,-0.8,-2.82820063659975E-17));
#4989=CARTESIAN_POINT('Origin',(0.115470053837925,-0.5,0.2));
#4990=CARTESIAN_POINT('',(0.115470053837925,-0.5,0.2));
#4991=CARTESIAN_POINT('',(-0.115470053837925,-0.5,0.2));
#4992=CARTESIAN_POINT('',(0.115470053837925,-0.8,0.2));
#4993=CARTESIAN_POINT('',(0.115470053837925,-0.5,0.2));
#4994=CARTESIAN_POINT('',(-0.115470053837925,-0.8,0.2));
#4995=CARTESIAN_POINT('Origin',(0.23094010767585,-0.5,0.));
#4996=CARTESIAN_POINT('',(0.115470053837925,-0.5,0.2));
#4997=CARTESIAN_POINT('',(0.115470053837925,-0.8,0.2));
#4998=CARTESIAN_POINT('Origin',(0.,-0.5,0.));
#4999=CARTESIAN_POINT('Origin',(0.,-0.8,0.));
#5000=CARTESIAN_POINT('Origin',(0.,-1.4,0.));
#5001=CARTESIAN_POINT('',(-0.24505,-1.4,3.00099698131059E-17));
#5002=CARTESIAN_POINT('Origin',(0.,-1.4,0.));
#5003=CARTESIAN_POINT('Origin',(0.375,0.5,0.));
#5004=CARTESIAN_POINT('',(-0.375,0.5,-4.59242549680257E-17));
#5005=CARTESIAN_POINT('Origin',(0.,0.5,0.));
#5006=CARTESIAN_POINT('Origin',(0.,0.475,0.));
#5007=CARTESIAN_POINT('',(-0.425,0.45,-5.20474889637625E-17));
#5008=CARTESIAN_POINT('Origin',(0.,0.45,0.));
#5009=CARTESIAN_POINT('',(-0.4,0.475,-4.89858719658941E-17));
#5010=CARTESIAN_POINT('Origin',(0.,0.24,0.));
#5011=CARTESIAN_POINT('',(-0.425,0.0299999999999998,-5.20474889637625E-17));
#5012=CARTESIAN_POINT('Origin',(0.,0.0299999999999998,0.));
#5013=CARTESIAN_POINT('',(-0.425,0.24,-5.20474889637625E-17));
#5014=CARTESIAN_POINT('Origin',(0.,0.0150000000000001,0.));
#5015=CARTESIAN_POINT('',(-0.395,4.85722573273506E-17,-4.83735485663204E-17));
#5016=CARTESIAN_POINT('Origin',(0.,0.,0.));
#5017=CARTESIAN_POINT('',(-0.41,0.0150000000000001,-5.02105187650415E-17));
#5018=CARTESIAN_POINT('Origin',(0.27,0.,0.));
#5019=CARTESIAN_POINT('',(-0.27,0.,-3.30654635769785E-17));
#5020=CARTESIAN_POINT('Origin',(0.,0.,0.));
#5021=CARTESIAN_POINT('Origin',(0.,-0.02,0.));
#5022=CARTESIAN_POINT('',(-0.24505,-0.0498999999999999,3.00099698131059E-17));
#5023=CARTESIAN_POINT('Origin',(0.,-0.0498999999999999,0.));
#5024=CARTESIAN_POINT('',(-0.26,-0.02,-3.18408167778312E-17));
#5025=CARTESIAN_POINT('Origin',(0.,-0.995,0.));
#5026=CARTESIAN_POINT('',(-0.24505,-0.995,-3.00099698131059E-17));
#5465=UNCERTAINTY_MEASURE_WITH_UNIT(LENGTH_MEASURE(0.001),#5493,
'DISTANCE_ACCURACY_VALUE',
'Maximum model space distance between geometric entities at asserted c
onnectivities');
#5475=UNCERTAINTY_MEASURE_WITH_UNIT(LENGTH_MEASURE(0.001),#5493,
'DISTANCE_ACCURACY_VALUE',
'Maximum model space distance between geometric entities at asserted c
onnectivities');
#5482=(
GEOMETRIC_REPRESENTATION_CONTEXT(3)
GLOBAL_UNCERTAINTY_ASSIGNED_CONTEXT((#5465))
GLOBAL_UNIT_ASSIGNED_CONTEXT((#5493,#5495,#5496))
REPRESENTATION_CONTEXT('','3D')
);
#5492=(
GEOMETRIC_REPRESENTATION_CONTEXT(3)
GLOBAL_UNCERTAINTY_ASSIGNED_CONTEXT((#5475))
GLOBAL_UNIT_ASSIGNED_CONTEXT((#5493,#5495,#5496))
REPRESENTATION_CONTEXT('','3D')
);
#5493=(
LENGTH_UNIT()
NAMED_UNIT(*)
SI_UNIT(.CENTI.,.METRE.)
);
#5495=(
NAMED_UNIT(*)
PLANE_ANGLE_UNIT()
SI_UNIT($,.RADIAN.)
);
#5496=(
NAMED_UNIT(*)
SI_UNIT($,.STERADIAN.)
SOLID_ANGLE_UNIT()
);
#5503=SHAPE_DEFINITION_REPRESENTATION(#5519,#5568);
#5519=PRODUCT_DEFINITION_SHAPE('',$,#5585);
#5568=SHAPE_REPRESENTATION('',(#3409),#5482);
#5578=PRODUCT_DEFINITION_CONTEXT('part definition',#5628,'design');
#5585=PRODUCT_DEFINITION('M5x14 Cap Screw','M5x14 Cap Screw',#5601,#5578);
#5601=PRODUCT_DEFINITION_FORMATION('',$,#5636);
#5628=APPLICATION_CONTEXT(
'Core Data for Automotive Mechanical Design Process');
#5629=PRODUCT_CONTEXT('part definition',#5628,'mechanical');
#5636=PRODUCT('M5x14 Cap Screw','M5x14 Cap Screw','M5x14 Cap Screw',(#5629));
#5702=COLOUR_RGB('Black',0.12,0.14,0.17);
#5703=FILL_AREA_STYLE_COLOUR('',#5702);
#5704=FILL_AREA_STYLE('',(#5703));
#5705=SURFACE_STYLE_FILL_AREA(#5704);
#5706=SURFACE_SIDE_STYLE('',(#5705));
#5707=SURFACE_STYLE_USAGE(.BOTH.,#5706);
#5708=PRESENTATION_STYLE_ASSIGNMENT((#5707));
ENDSEC;
END-ISO-10303-21;
